ISO-10303-21;
HEADER;
/* Generated by software containing ST-Developer
 * from STEP Tools, Inc. (www.steptools.com) 
 */

FILE_DESCRIPTION(
/* description */ ('PAT-122'),
/* implementation_level */ '2;1');

FILE_NAME(
/* name */ 'Bonded foot pad (3).step',
/* time_stamp */ '2026-10-29T20:20:12-07:00',
/* author */ (''),
/* organization */ (''),
/* preprocessor_version */ 'ST-DEVELOPER v20.2',
/* originating_system */ 'Autodesk Translation Framework v15.17.0.0',
/* authorisation */ '');

FILE_SCHEMA (('AUTOMOTIVE_DESIGN { 1 0 10303 214 3 1 1 }'));
ENDSEC;

DATA;
#10=MECHANICAL_DESIGN_GEOMETRIC_PRESENTATION_REPRESENTATION('',(#498),#10019);
#454=SHAPE_REPRESENTATION_RELATIONSHIP('SRR','None',#10175,#476);
#476=ADVANCED_BREP_SHAPE_REPRESENTATION('',(#520),#10004);
#498=STYLED_ITEM('',(#10341),#520);
#520=MANIFOLD_SOLID_BREP('Body1',#5620);
#545=FACE_BOUND('',#1162,.T.);
#546=FACE_BOUND('',#1164,.T.);
#623=PLANE('',#5953);
#624=PLANE('',#5954);
#853=FACE_OUTER_BOUND('',#1159,.T.);
#854=FACE_OUTER_BOUND('',#1160,.T.);
#855=FACE_OUTER_BOUND('',#1161,.T.);
#856=FACE_OUTER_BOUND('',#1163,.T.);
#1159=EDGE_LOOP('',(#3949,#3950,#3951,#3952));
#1160=EDGE_LOOP('',(#3953,#3954,#3955,#3956));
#1161=EDGE_LOOP('',(#3957));
#1162=EDGE_LOOP('',(#3958));
#1163=EDGE_LOOP('',(#3959));
#1164=EDGE_LOOP('',(#3960));
#1501=LINE('',#8169,#2045);
#1502=LINE('',#8175,#2046);
#2045=VECTOR('',#6574,0.600000000000001);
#2046=VECTOR('',#6581,2.);
#2603=CIRCLE('',#5948,0.600000000000001);
#2604=CIRCLE('',#5949,0.600000000000001);
#2605=CIRCLE('',#5951,2.);
#2606=CIRCLE('',#5952,2.);
#2733=VERTEX_POINT('',#8166);
#2734=VERTEX_POINT('',#8168);
#2735=VERTEX_POINT('',#8172);
#2736=VERTEX_POINT('',#8174);
#3209=EDGE_CURVE('',#2733,#2733,#2603,.T.);
#3210=EDGE_CURVE('',#2733,#2734,#1501,.T.);
#3211=EDGE_CURVE('',#2734,#2734,#2604,.T.);
#3212=EDGE_CURVE('',#2735,#2735,#2605,.T.);
#3213=EDGE_CURVE('',#2735,#2736,#1502,.T.);
#3214=EDGE_CURVE('',#2736,#2736,#2606,.T.);
#3949=ORIENTED_EDGE('',*,*,#3209,.F.);
#3950=ORIENTED_EDGE('',*,*,#3210,.T.);
#3951=ORIENTED_EDGE('',*,*,#3211,.T.);
#3952=ORIENTED_EDGE('',*,*,#3210,.F.);
#3953=ORIENTED_EDGE('',*,*,#3212,.F.);
#3954=ORIENTED_EDGE('',*,*,#3213,.T.);
#3955=ORIENTED_EDGE('',*,*,#3214,.T.);
#3956=ORIENTED_EDGE('',*,*,#3213,.F.);
#3957=ORIENTED_EDGE('',*,*,#3212,.T.);
#3958=ORIENTED_EDGE('',*,*,#3209,.T.);
#3959=ORIENTED_EDGE('',*,*,#3214,.F.);
#3960=ORIENTED_EDGE('',*,*,#3211,.F.);
#5275=CYLINDRICAL_SURFACE('',#5947,0.600000000000001);
#5276=CYLINDRICAL_SURFACE('',#5950,2.);
#5349=ADVANCED_FACE('',(#853),#5275,.F.);
#5350=ADVANCED_FACE('',(#854),#5276,.T.);
#5351=ADVANCED_FACE('',(#855,#545),#623,.T.);
#5352=ADVANCED_FACE('',(#856,#546),#624,.F.);
#5620=CLOSED_SHELL('',(#5349,#5350,#5351,#5352));
#5946=AXIS2_PLACEMENT_3D('',#8164,#6568,#6569);
#5947=AXIS2_PLACEMENT_3D('',#8165,#6570,#6571);
#5948=AXIS2_PLACEMENT_3D('',#8167,#6572,#6573);
#5949=AXIS2_PLACEMENT_3D('',#8170,#6575,#6576);
#5950=AXIS2_PLACEMENT_3D('',#8171,#6577,#6578);
#5951=AXIS2_PLACEMENT_3D('',#8173,#6579,#6580);
#5952=AXIS2_PLACEMENT_3D('',#8176,#6582,#6583);
#5953=AXIS2_PLACEMENT_3D('',#8177,#6584,#6585);
#5954=AXIS2_PLACEMENT_3D('',#8178,#6586,#6587);
#6568=DIRECTION('axis',(0.,0.,1.));
#6569=DIRECTION('refdir',(1.,0.,0.));
#6570=DIRECTION('center_axis',(0.,0.,1.));
#6571=DIRECTION('ref_axis',(1.,0.,0.));
#6572=DIRECTION('center_axis',(0.,0.,-1.));
#6573=DIRECTION('ref_axis',(1.,0.,0.));
#6574=DIRECTION('',(0.,0.,-1.));
#6575=DIRECTION('center_axis',(0.,0.,-1.));
#6576=DIRECTION('ref_axis',(1.,0.,0.));
#6577=DIRECTION('center_axis',(0.,0.,1.));
#6578=DIRECTION('ref_axis',(1.,0.,0.));
#6579=DIRECTION('center_axis',(0.,0.,1.));
#6580=DIRECTION('ref_axis',(1.,0.,0.));
#6581=DIRECTION('',(0.,0.,-1.));
#6582=DIRECTION('center_axis',(0.,0.,1.));
#6583=DIRECTION('ref_axis',(1.,0.,0.));
#6584=DIRECTION('center_axis',(0.,0.,1.));
#6585=DIRECTION('ref_axis',(1.,0.,0.));
#6586=DIRECTION('center_axis',(0.,0.,1.));
#6587=DIRECTION('ref_axis',(1.,0.,0.));
#8164=CARTESIAN_POINT('',(0.,0.,0.));
#8165=CARTESIAN_POINT('Origin',(19.,19.,-1.6));
#8166=CARTESIAN_POINT('',(18.4,19.,-0.8));
#8167=CARTESIAN_POINT('Origin',(19.,19.,-0.8));
#8168=CARTESIAN_POINT('',(18.4,19.,-1.6));
#8169=CARTESIAN_POINT('',(18.4,19.,-1.6));
#8170=CARTESIAN_POINT('Origin',(19.,19.,-1.6));
#8171=CARTESIAN_POINT('Origin',(19.,19.,-1.6));
#8172=CARTESIAN_POINT('',(17.,19.,-0.8));
#8173=CARTESIAN_POINT('Origin',(19.,19.,-0.8));
#8174=CARTESIAN_POINT('',(17.,19.,-1.6));
#8175=CARTESIAN_POINT('',(17.,19.,-1.6));
#8176=CARTESIAN_POINT('Origin',(19.,19.,-1.6));
#8177=CARTESIAN_POINT('Origin',(19.,19.,-0.8));
#8178=CARTESIAN_POINT('Origin',(19.,19.,-1.6));
#9980=UNCERTAINTY_MEASURE_WITH_UNIT(LENGTH_MEASURE(0.001),#10020,
'DISTANCE_ACCURACY_VALUE',
'Maximum model space distance between geometric entities at asserted c
onnectivities');
#9995=UNCERTAINTY_MEASURE_WITH_UNIT(LENGTH_MEASURE(0.001),#10020,
'DISTANCE_ACCURACY_VALUE',
'Maximum model space distance between geometric entities at asserted c
onnectivities');
#10004=(
GEOMETRIC_REPRESENTATION_CONTEXT(3)
GLOBAL_UNCERTAINTY_ASSIGNED_CONTEXT((#9980))
GLOBAL_UNIT_ASSIGNED_CONTEXT((#10020,#10022,#10023))
REPRESENTATION_CONTEXT('','3D')
);
#10019=(
GEOMETRIC_REPRESENTATION_CONTEXT(3)
GLOBAL_UNCERTAINTY_ASSIGNED_CONTEXT((#9995))
GLOBAL_UNIT_ASSIGNED_CONTEXT((#10020,#10022,#10023))
REPRESENTATION_CONTEXT('','3D')
);
#10020=(
LENGTH_UNIT()
NAMED_UNIT(*)
SI_UNIT(.CENTI.,.METRE.)
);
#10022=(
NAMED_UNIT(*)
PLANE_ANGLE_UNIT()
SI_UNIT($,.RADIAN.)
);
#10023=(
NAMED_UNIT(*)
SI_UNIT($,.STERADIAN.)
SOLID_ANGLE_UNIT()
);
#10032=SHAPE_DEFINITION_REPRESENTATION(#10055,#10175);
#10055=PRODUCT_DEFINITION_SHAPE('',$,#10199);
#10175=SHAPE_REPRESENTATION('',(#5946),#10004);
#10190=PRODUCT_DEFINITION_CONTEXT('part definition',#10261,'design');
#10199=PRODUCT_DEFINITION('Bonded foot pad (3)',
'Bonded foot pad (3)',#10222,#10190);
#10222=PRODUCT_DEFINITION_FORMATION('',$,#10271);
#10261=APPLICATION_CONTEXT(
'Core Data for Automotive Mechanical Design Process');
#10262=PRODUCT_CONTEXT('part definition',#10261,'mechanical');
#10271=PRODUCT('Bonded foot pad (3)','Bonded foot pad (3)',
'Bonded foot pad (3)',(#10262));
#10335=COLOUR_RGB('Sky Blue',0.24,0.69,0.87);
#10336=FILL_AREA_STYLE_COLOUR('',#10335);
#10337=FILL_AREA_STYLE('',(#10336));
#10338=SURFACE_STYLE_FILL_AREA(#10337);
#10339=SURFACE_SIDE_STYLE('',(#10338));
#10340=SURFACE_STYLE_USAGE(.BOTH.,#10339);
#10341=PRESENTATION_STYLE_ASSIGNMENT((#10340));
ENDSEC;
END-ISO-10303-21;
